ISO-10303-21;
HEADER;
/* Generated by software containing ST-Developer
 * from STEP Tools, Inc. (www.steptools.com) 
 */

FILE_DESCRIPTION(
/* description */ ('Manifold and mounting hardware'),
/* implementation_level */ '2;1');

FILE_NAME(
/* name */ '1_4-1_8 in port reducer (2).step',
/* time_stamp */ '2026-10-28T21:46:49-07:00',
/* author */ (''),
/* organization */ (''),
/* preprocessor_version */ 'ST-DEVELOPER v20.2',
/* originating_system */ 'Autodesk Translation Framework v15.17.0.0',
/* authorisation */ '');

FILE_SCHEMA (('AUTOMOTIVE_DESIGN { 1 0 10303 214 3 1 1 }'));
ENDSEC;

DATA;
#10=MECHANICAL_DESIGN_GEOMETRIC_PRESENTATION_REPRESENTATION('',(#154),#5638);
#126=SHAPE_REPRESENTATION_RELATIONSHIP('SRR','None',#5705,#140);
#140=ADVANCED_BREP_SHAPE_REPRESENTATION('',(#168),#5627);
#154=STYLED_ITEM('',(#5853),#168);
#168=MANIFOLD_SOLID_BREP('Body1',#3144);
#208=FACE_BOUND('',#624,.T.);
#209=FACE_BOUND('',#626,.T.);
#210=FACE_BOUND('',#634,.T.);
#211=FACE_BOUND('',#638,.T.);
#297=CYLINDRICAL_SURFACE('',#3457,0.515);
#298=CYLINDRICAL_SURFACE('',#3471,0.2);
#299=CYLINDRICAL_SURFACE('',#3473,0.685);
#406=FACE_OUTER_BOUND('',#622,.T.);
#407=FACE_OUTER_BOUND('',#623,.T.);
#408=FACE_OUTER_BOUND('',#625,.T.);
#409=FACE_OUTER_BOUND('',#627,.T.);
#410=FACE_OUTER_BOUND('',#628,.T.);
#411=FACE_OUTER_BOUND('',#629,.T.);
#412=FACE_OUTER_BOUND('',#630,.T.);
#413=FACE_OUTER_BOUND('',#631,.T.);
#414=FACE_OUTER_BOUND('',#632,.T.);
#415=FACE_OUTER_BOUND('',#633,.T.);
#416=FACE_OUTER_BOUND('',#635,.T.);
#417=FACE_OUTER_BOUND('',#636,.T.);
#418=FACE_OUTER_BOUND('',#637,.T.);
#622=EDGE_LOOP('',(#2388,#2389,#2390,#2391));
#623=EDGE_LOOP('',(#2392));
#624=EDGE_LOOP('',(#2393));
#625=EDGE_LOOP('',(#2394,#2395,#2396,#2397,#2398,#2399));
#626=EDGE_LOOP('',(#2400));
#627=EDGE_LOOP('',(#2401,#2402,#2403,#2404));
#628=EDGE_LOOP('',(#2405,#2406,#2407,#2408));
#629=EDGE_LOOP('',(#2409,#2410,#2411,#2412));
#630=EDGE_LOOP('',(#2413,#2414,#2415,#2416));
#631=EDGE_LOOP('',(#2417,#2418,#2419,#2420));
#632=EDGE_LOOP('',(#2421,#2422,#2423,#2424));
#633=EDGE_LOOP('',(#2425,#2426,#2427,#2428,#2429,#2430));
#634=EDGE_LOOP('',(#2431));
#635=EDGE_LOOP('',(#2432,#2433,#2434,#2435));
#636=EDGE_LOOP('',(#2436,#2437,#2438,#2439));
#637=EDGE_LOOP('',(#2440));
#638=EDGE_LOOP('',(#2441));
#827=CIRCLE('',#3458,0.515);
#828=CIRCLE('',#3459,0.515);
#829=CIRCLE('',#3461,0.2);
#830=CIRCLE('',#3463,0.685);
#831=CIRCLE('',#3472,0.2);
#832=CIRCLE('',#3474,0.685);
#999=LINE('',#5085,#1246);
#1000=LINE('',#5093,#1247);
#1001=LINE('',#5095,#1248);
#1002=LINE('',#5097,#1249);
#1003=LINE('',#5099,#1250);
#1004=LINE('',#5101,#1251);
#1005=LINE('',#5102,#1252);
#1006=LINE('',#5107,#1253);
#1007=LINE('',#5109,#1254);
#1008=LINE('',#5110,#1255);
#1009=LINE('',#5113,#1256);
#1010=LINE('',#5114,#1257);
#1011=LINE('',#5117,#1258);
#1012=LINE('',#5118,#1259);
#1013=LINE('',#5121,#1260);
#1014=LINE('',#5122,#1261);
#1015=LINE('',#5125,#1262);
#1016=LINE('',#5126,#1263);
#1017=LINE('',#5128,#1264);
#1018=LINE('',#5132,#1265);
#1019=LINE('',#5136,#1266);
#1246=VECTOR('',#4074,0.515);
#1247=VECTOR('',#4083,1.);
#1248=VECTOR('',#4084,1.);
#1249=VECTOR('',#4085,1.);
#1250=VECTOR('',#4086,1.);
#1251=VECTOR('',#4087,1.);
#1252=VECTOR('',#4088,1.);
#1253=VECTOR('',#4093,1.);
#1254=VECTOR('',#4094,1.);
#1255=VECTOR('',#4095,1.);
#1256=VECTOR('',#4098,1.);
#1257=VECTOR('',#4099,1.);
#1258=VECTOR('',#4102,1.);
#1259=VECTOR('',#4103,1.);
#1260=VECTOR('',#4106,1.);
#1261=VECTOR('',#4107,1.);
#1262=VECTOR('',#4110,1.);
#1263=VECTOR('',#4111,1.);
#1264=VECTOR('',#4114,1.);
#1265=VECTOR('',#4119,0.2);
#1266=VECTOR('',#4124,0.685);
#1505=VERTEX_POINT('',#5082);
#1506=VERTEX_POINT('',#5084);
#1507=VERTEX_POINT('',#5088);
#1508=VERTEX_POINT('',#5091);
#1509=VERTEX_POINT('',#5092);
#1510=VERTEX_POINT('',#5094);
#1511=VERTEX_POINT('',#5096);
#1512=VERTEX_POINT('',#5098);
#1513=VERTEX_POINT('',#5100);
#1514=VERTEX_POINT('',#5103);
#1515=VERTEX_POINT('',#5106);
#1516=VERTEX_POINT('',#5108);
#1517=VERTEX_POINT('',#5112);
#1518=VERTEX_POINT('',#5116);
#1519=VERTEX_POINT('',#5120);
#1520=VERTEX_POINT('',#5124);
#1521=VERTEX_POINT('',#5131);
#1522=VERTEX_POINT('',#5135);
#1823=EDGE_CURVE('',#1505,#1505,#827,.T.);
#1824=EDGE_CURVE('',#1505,#1506,#999,.T.);
#1825=EDGE_CURVE('',#1506,#1506,#828,.T.);
#1826=EDGE_CURVE('',#1507,#1507,#829,.T.);
#1827=EDGE_CURVE('',#1508,#1509,#1000,.T.);
#1828=EDGE_CURVE('',#1510,#1508,#1001,.T.);
#1829=EDGE_CURVE('',#1511,#1510,#1002,.T.);
#1830=EDGE_CURVE('',#1512,#1511,#1003,.T.);
#1831=EDGE_CURVE('',#1513,#1512,#1004,.T.);
#1832=EDGE_CURVE('',#1509,#1513,#1005,.T.);
#1833=EDGE_CURVE('',#1514,#1514,#830,.T.);
#1834=EDGE_CURVE('',#1508,#1515,#1006,.T.);
#1835=EDGE_CURVE('',#1516,#1515,#1007,.T.);
#1836=EDGE_CURVE('',#1510,#1516,#1008,.T.);
#1837=EDGE_CURVE('',#1517,#1516,#1009,.T.);
#1838=EDGE_CURVE('',#1511,#1517,#1010,.T.);
#1839=EDGE_CURVE('',#1518,#1517,#1011,.T.);
#1840=EDGE_CURVE('',#1512,#1518,#1012,.T.);
#1841=EDGE_CURVE('',#1519,#1518,#1013,.T.);
#1842=EDGE_CURVE('',#1513,#1519,#1014,.T.);
#1843=EDGE_CURVE('',#1520,#1519,#1015,.T.);
#1844=EDGE_CURVE('',#1509,#1520,#1016,.T.);
#1845=EDGE_CURVE('',#1515,#1520,#1017,.T.);
#1846=EDGE_CURVE('',#1507,#1521,#1018,.T.);
#1847=EDGE_CURVE('',#1521,#1521,#831,.T.);
#1848=EDGE_CURVE('',#1514,#1522,#1019,.T.);
#1849=EDGE_CURVE('',#1522,#1522,#832,.T.);
#2388=ORIENTED_EDGE('',*,*,#1823,.F.);
#2389=ORIENTED_EDGE('',*,*,#1824,.T.);
#2390=ORIENTED_EDGE('',*,*,#1825,.F.);
#2391=ORIENTED_EDGE('',*,*,#1824,.F.);
#2392=ORIENTED_EDGE('',*,*,#1823,.T.);
#2393=ORIENTED_EDGE('',*,*,#1826,.F.);
#2394=ORIENTED_EDGE('',*,*,#1827,.F.);
#2395=ORIENTED_EDGE('',*,*,#1828,.F.);
#2396=ORIENTED_EDGE('',*,*,#1829,.F.);
#2397=ORIENTED_EDGE('',*,*,#1830,.F.);
#2398=ORIENTED_EDGE('',*,*,#1831,.F.);
#2399=ORIENTED_EDGE('',*,*,#1832,.F.);
#2400=ORIENTED_EDGE('',*,*,#1833,.T.);
#2401=ORIENTED_EDGE('',*,*,#1828,.T.);
#2402=ORIENTED_EDGE('',*,*,#1834,.T.);
#2403=ORIENTED_EDGE('',*,*,#1835,.F.);
#2404=ORIENTED_EDGE('',*,*,#1836,.F.);
#2405=ORIENTED_EDGE('',*,*,#1829,.T.);
#2406=ORIENTED_EDGE('',*,*,#1836,.T.);
#2407=ORIENTED_EDGE('',*,*,#1837,.F.);
#2408=ORIENTED_EDGE('',*,*,#1838,.F.);
#2409=ORIENTED_EDGE('',*,*,#1830,.T.);
#2410=ORIENTED_EDGE('',*,*,#1838,.T.);
#2411=ORIENTED_EDGE('',*,*,#1839,.F.);
#2412=ORIENTED_EDGE('',*,*,#1840,.F.);
#2413=ORIENTED_EDGE('',*,*,#1831,.T.);
#2414=ORIENTED_EDGE('',*,*,#1840,.T.);
#2415=ORIENTED_EDGE('',*,*,#1841,.F.);
#2416=ORIENTED_EDGE('',*,*,#1842,.F.);
#2417=ORIENTED_EDGE('',*,*,#1832,.T.);
#2418=ORIENTED_EDGE('',*,*,#1842,.T.);
#2419=ORIENTED_EDGE('',*,*,#1843,.F.);
#2420=ORIENTED_EDGE('',*,*,#1844,.F.);
#2421=ORIENTED_EDGE('',*,*,#1827,.T.);
#2422=ORIENTED_EDGE('',*,*,#1844,.T.);
#2423=ORIENTED_EDGE('',*,*,#1845,.F.);
#2424=ORIENTED_EDGE('',*,*,#1834,.F.);
#2425=ORIENTED_EDGE('',*,*,#1845,.T.);
#2426=ORIENTED_EDGE('',*,*,#1843,.T.);
#2427=ORIENTED_EDGE('',*,*,#1841,.T.);
#2428=ORIENTED_EDGE('',*,*,#1839,.T.);
#2429=ORIENTED_EDGE('',*,*,#1837,.T.);
#2430=ORIENTED_EDGE('',*,*,#1835,.T.);
#2431=ORIENTED_EDGE('',*,*,#1825,.T.);
#2432=ORIENTED_EDGE('',*,*,#1826,.T.);
#2433=ORIENTED_EDGE('',*,*,#1846,.T.);
#2434=ORIENTED_EDGE('',*,*,#1847,.T.);
#2435=ORIENTED_EDGE('',*,*,#1846,.F.);
#2436=ORIENTED_EDGE('',*,*,#1833,.F.);
#2437=ORIENTED_EDGE('',*,*,#1848,.T.);
#2438=ORIENTED_EDGE('',*,*,#1849,.T.);
#2439=ORIENTED_EDGE('',*,*,#1848,.F.);
#2440=ORIENTED_EDGE('',*,*,#1849,.F.);
#2441=ORIENTED_EDGE('',*,*,#1847,.F.);
#2882=PLANE('',#3460);
#2883=PLANE('',#3462);
#2884=PLANE('',#3464);
#2885=PLANE('',#3465);
#2886=PLANE('',#3466);
#2887=PLANE('',#3467);
#2888=PLANE('',#3468);
#2889=PLANE('',#3469);
#2890=PLANE('',#3470);
#2891=PLANE('',#3475);
#3030=ADVANCED_FACE('',(#406),#297,.F.);
#3031=ADVANCED_FACE('',(#407,#208),#2882,.T.);
#3032=ADVANCED_FACE('',(#408,#209),#2883,.F.);
#3033=ADVANCED_FACE('',(#409),#2884,.T.);
#3034=ADVANCED_FACE('',(#410),#2885,.T.);
#3035=ADVANCED_FACE('',(#411),#2886,.T.);
#3036=ADVANCED_FACE('',(#412),#2887,.T.);
#3037=ADVANCED_FACE('',(#413),#2888,.T.);
#3038=ADVANCED_FACE('',(#414),#2889,.T.);
#3039=ADVANCED_FACE('',(#415,#210),#2890,.T.);
#3040=ADVANCED_FACE('',(#416),#298,.F.);
#3041=ADVANCED_FACE('',(#417),#299,.T.);
#3042=ADVANCED_FACE('',(#418,#211),#2891,.F.);
#3144=CLOSED_SHELL('',(#3030,#3031,#3032,#3033,#3034,#3035,#3036,#3037,
#3038,#3039,#3040,#3041,#3042));
#3456=AXIS2_PLACEMENT_3D('',#5080,#4068,#4069);
#3457=AXIS2_PLACEMENT_3D('',#5081,#4070,#4071);
#3458=AXIS2_PLACEMENT_3D('',#5083,#4072,#4073);
#3459=AXIS2_PLACEMENT_3D('',#5086,#4075,#4076);
#3460=AXIS2_PLACEMENT_3D('',#5087,#4077,#4078);
#3461=AXIS2_PLACEMENT_3D('',#5089,#4079,#4080);
#3462=AXIS2_PLACEMENT_3D('',#5090,#4081,#4082);
#3463=AXIS2_PLACEMENT_3D('',#5104,#4089,#4090);
#3464=AXIS2_PLACEMENT_3D('',#5105,#4091,#4092);
#3465=AXIS2_PLACEMENT_3D('',#5111,#4096,#4097);
#3466=AXIS2_PLACEMENT_3D('',#5115,#4100,#4101);
#3467=AXIS2_PLACEMENT_3D('',#5119,#4104,#4105);
#3468=AXIS2_PLACEMENT_3D('',#5123,#4108,#4109);
#3469=AXIS2_PLACEMENT_3D('',#5127,#4112,#4113);
#3470=AXIS2_PLACEMENT_3D('',#5129,#4115,#4116);
#3471=AXIS2_PLACEMENT_3D('',#5130,#4117,#4118);
#3472=AXIS2_PLACEMENT_3D('',#5133,#4120,#4121);
#3473=AXIS2_PLACEMENT_3D('',#5134,#4122,#4123);
#3474=AXIS2_PLACEMENT_3D('',#5137,#4125,#4126);
#3475=AXIS2_PLACEMENT_3D('',#5138,#4127,#4128);
#4068=DIRECTION('axis',(0.,0.,1.));
#4069=DIRECTION('refdir',(1.,0.,0.));
#4070=DIRECTION('center_axis',(0.,0.,1.));
#4071=DIRECTION('ref_axis',(1.,0.,0.));
#4072=DIRECTION('center_axis',(0.,0.,1.));
#4073=DIRECTION('ref_axis',(1.,0.,0.));
#4074=DIRECTION('',(0.,0.,1.));
#4075=DIRECTION('center_axis',(0.,0.,-1.));
#4076=DIRECTION('ref_axis',(1.,0.,0.));
#4077=DIRECTION('center_axis',(0.,0.,1.));
#4078=DIRECTION('ref_axis',(1.,0.,0.));
#4079=DIRECTION('center_axis',(0.,0.,1.));
#4080=DIRECTION('ref_axis',(1.,0.,0.));
#4081=DIRECTION('center_axis',(0.,0.,1.));
#4082=DIRECTION('ref_axis',(1.,0.,0.));
#4083=DIRECTION('',(0.5,0.866025403784439,0.));
#4084=DIRECTION('',(1.,-3.29650746237182E-16,0.));
#4085=DIRECTION('',(0.5,-0.866025403784439,0.));
#4086=DIRECTION('',(-0.5,-0.866025403784438,0.));
#4087=DIRECTION('',(-1.,0.,0.));
#4088=DIRECTION('',(-0.5,0.866025403784439,0.));
#4089=DIRECTION('center_axis',(0.,0.,1.));
#4090=DIRECTION('ref_axis',(1.,0.,0.));
#4091=DIRECTION('center_axis',(-3.29650746237182E-16,-1.,0.));
#4092=DIRECTION('ref_axis',(1.,-3.29650746237182E-16,0.));
#4093=DIRECTION('',(0.,0.,1.));
#4094=DIRECTION('',(1.,-3.29650746237182E-16,0.));
#4095=DIRECTION('',(0.,0.,1.));
#4096=DIRECTION('center_axis',(-0.866025403784439,-0.5,0.));
#4097=DIRECTION('ref_axis',(0.5,-0.866025403784439,0.));
#4098=DIRECTION('',(0.5,-0.866025403784439,0.));
#4099=DIRECTION('',(0.,0.,1.));
#4100=DIRECTION('center_axis',(-0.866025403784438,0.5,0.));
#4101=DIRECTION('ref_axis',(-0.5,-0.866025403784438,0.));
#4102=DIRECTION('',(-0.5,-0.866025403784438,0.));
#4103=DIRECTION('',(0.,0.,1.));
#4104=DIRECTION('center_axis',(0.,1.,0.));
#4105=DIRECTION('ref_axis',(-1.,0.,0.));
#4106=DIRECTION('',(-1.,0.,0.));
#4107=DIRECTION('',(0.,0.,1.));
#4108=DIRECTION('center_axis',(0.866025403784439,0.5,0.));
#4109=DIRECTION('ref_axis',(-0.5,0.866025403784439,0.));
#4110=DIRECTION('',(-0.5,0.866025403784439,0.));
#4111=DIRECTION('',(0.,0.,1.));
#4112=DIRECTION('center_axis',(0.866025403784439,-0.5,0.));
#4113=DIRECTION('ref_axis',(0.5,0.866025403784439,0.));
#4114=DIRECTION('',(0.5,0.866025403784439,0.));
#4115=DIRECTION('center_axis',(0.,0.,1.));
#4116=DIRECTION('ref_axis',(1.,0.,0.));
#4117=DIRECTION('center_axis',(0.,0.,1.));
#4118=DIRECTION('ref_axis',(1.,0.,0.));
#4119=DIRECTION('',(0.,0.,-1.));
#4120=DIRECTION('center_axis',(0.,0.,-1.));
#4121=DIRECTION('ref_axis',(1.,0.,0.));
#4122=DIRECTION('center_axis',(0.,0.,1.));
#4123=DIRECTION('ref_axis',(1.,0.,0.));
#4124=DIRECTION('',(0.,0.,-1.));
#4125=DIRECTION('center_axis',(0.,0.,1.));
#4126=DIRECTION('ref_axis',(1.,0.,0.));
#4127=DIRECTION('center_axis',(0.,0.,1.));
#4128=DIRECTION('ref_axis',(1.,0.,0.));
#5080=CARTESIAN_POINT('',(0.,0.,0.));
#5081=CARTESIAN_POINT('Origin',(3.75,0.,4.85));
#5082=CARTESIAN_POINT('',(3.235,-6.30693101560886E-17,4.85));
#5083=CARTESIAN_POINT('Origin',(3.75,0.,4.85));
#5084=CARTESIAN_POINT('',(3.235,6.30693101560886E-17,5.5));
#5085=CARTESIAN_POINT('',(3.235,-6.30693101560886E-17,4.85));
#5086=CARTESIAN_POINT('Origin',(3.75,0.,5.5));
#5087=CARTESIAN_POINT('Origin',(3.75,0.,4.85));
#5088=CARTESIAN_POINT('',(3.55,-2.44929359829471E-17,4.85));
#5089=CARTESIAN_POINT('Origin',(3.75,0.,4.85));
#5090=CARTESIAN_POINT('Origin',(3.75,0.,5.));
#5091=CARTESIAN_POINT('',(4.25518148554092,-0.875,5.));
#5092=CARTESIAN_POINT('',(4.76036297108184,0.,5.));
#5093=CARTESIAN_POINT('',(4.25518148554092,-0.875,5.));
#5094=CARTESIAN_POINT('',(3.24481851445908,-0.875,5.));
#5095=CARTESIAN_POINT('',(3.24481851445908,-0.875,5.));
#5096=CARTESIAN_POINT('',(2.73963702891815,1.23733777851239E-16,5.));
#5097=CARTESIAN_POINT('',(2.73963702891815,1.23733777851239E-16,5.));
#5098=CARTESIAN_POINT('',(3.24481851445908,0.875,5.));
#5099=CARTESIAN_POINT('',(3.24481851445908,0.875,5.));
#5100=CARTESIAN_POINT('',(4.25518148554092,0.875,5.));
#5101=CARTESIAN_POINT('',(4.25518148554092,0.875,5.));
#5102=CARTESIAN_POINT('',(4.76036297108184,0.,5.));
#5103=CARTESIAN_POINT('',(3.065,-8.38883057415936E-17,5.));
#5104=CARTESIAN_POINT('Origin',(3.75,0.,5.));
#5105=CARTESIAN_POINT('Origin',(3.24481851445908,-0.875,5.));
#5106=CARTESIAN_POINT('',(4.25518148554092,-0.875,5.5));
#5107=CARTESIAN_POINT('',(4.25518148554092,-0.875,5.));
#5108=CARTESIAN_POINT('',(3.24481851445908,-0.875,5.5));
#5109=CARTESIAN_POINT('',(3.24481851445908,-0.875,5.5));
#5110=CARTESIAN_POINT('',(3.24481851445908,-0.875,5.));
#5111=CARTESIAN_POINT('Origin',(2.73963702891815,1.23733777851239E-16,5.));
#5112=CARTESIAN_POINT('',(2.73963702891815,1.11022302462516E-16,5.5));
#5113=CARTESIAN_POINT('',(2.73963702891815,1.23733777851239E-16,5.5));
#5114=CARTESIAN_POINT('',(2.73963702891815,1.23733777851239E-16,5.));
#5115=CARTESIAN_POINT('Origin',(3.24481851445908,0.875,5.));
#5116=CARTESIAN_POINT('',(3.24481851445908,0.875,5.5));
#5117=CARTESIAN_POINT('',(3.24481851445908,0.875,5.5));
#5118=CARTESIAN_POINT('',(3.24481851445908,0.875,5.));
#5119=CARTESIAN_POINT('Origin',(4.25518148554092,0.875,5.));
#5120=CARTESIAN_POINT('',(4.25518148554092,0.875,5.5));
#5121=CARTESIAN_POINT('',(4.25518148554092,0.875,5.5));
#5122=CARTESIAN_POINT('',(4.25518148554092,0.875,5.));
#5123=CARTESIAN_POINT('Origin',(4.76036297108184,0.,5.));
#5124=CARTESIAN_POINT('',(4.76036297108184,0.,5.5));
#5125=CARTESIAN_POINT('',(4.76036297108184,0.,5.5));
#5126=CARTESIAN_POINT('',(4.76036297108184,0.,5.));
#5127=CARTESIAN_POINT('Origin',(4.25518148554092,-0.875,5.));
#5128=CARTESIAN_POINT('',(4.25518148554092,-0.875,5.5));
#5129=CARTESIAN_POINT('Origin',(3.75,0.,5.5));
#5130=CARTESIAN_POINT('Origin',(3.75,0.,3.8));
#5131=CARTESIAN_POINT('',(3.55,-2.44929359829471E-17,3.8));
#5132=CARTESIAN_POINT('',(3.55,-2.44929359829471E-17,3.8));
#5133=CARTESIAN_POINT('Origin',(3.75,0.,3.8));
#5134=CARTESIAN_POINT('Origin',(3.75,0.,3.8));
#5135=CARTESIAN_POINT('',(3.065,-8.38883057415936E-17,3.8));
#5136=CARTESIAN_POINT('',(3.065,-8.38883057415936E-17,3.8));
#5137=CARTESIAN_POINT('Origin',(3.75,0.,3.8));
#5138=CARTESIAN_POINT('Origin',(3.75,0.,3.8));
#5610=UNCERTAINTY_MEASURE_WITH_UNIT(LENGTH_MEASURE(0.001),#5639,
'DISTANCE_ACCURACY_VALUE',
'Maximum model space distance between geometric entities at asserted c
onnectivities');
#5621=UNCERTAINTY_MEASURE_WITH_UNIT(LENGTH_MEASURE(0.001),#5639,
'DISTANCE_ACCURACY_VALUE',
'Maximum model space distance between geometric entities at asserted c
onnectivities');
#5627=(
GEOMETRIC_REPRESENTATION_CONTEXT(3)
GLOBAL_UNCERTAINTY_ASSIGNED_CONTEXT((#5610))
GLOBAL_UNIT_ASSIGNED_CONTEXT((#5639,#5641,#5642))
REPRESENTATION_CONTEXT('','3D')
);
#5638=(
GEOMETRIC_REPRESENTATION_CONTEXT(3)
GLOBAL_UNCERTAINTY_ASSIGNED_CONTEXT((#5621))
GLOBAL_UNIT_ASSIGNED_CONTEXT((#5639,#5641,#5642))
REPRESENTATION_CONTEXT('','3D')
);
#5639=(
LENGTH_UNIT()
NAMED_UNIT(*)
SI_UNIT(.CENTI.,.METRE.)
);
#5641=(
NAMED_UNIT(*)
PLANE_ANGLE_UNIT()
SI_UNIT($,.RADIAN.)
);
#5642=(
NAMED_UNIT(*)
SI_UNIT($,.STERADIAN.)
SOLID_ANGLE_UNIT()
);
#5648=SHAPE_DEFINITION_REPRESENTATION(#5664,#5705);
#5664=PRODUCT_DEFINITION_SHAPE('',$,#5722);
#5705=SHAPE_REPRESENTATION('',(#3456),#5627);
#5716=PRODUCT_DEFINITION_CONTEXT('part definition',#5766,'design');
#5722=PRODUCT_DEFINITION('1/4-1/8 in port reducer (2)',
'1/4-1/8 in port reducer (2)',#5738,#5716);
#5738=PRODUCT_DEFINITION_FORMATION('',$,#5773);
#5766=APPLICATION_CONTEXT(
'Core Data for Automotive Mechanical Design Process');
#5767=PRODUCT_CONTEXT('part definition',#5766,'mechanical');
#5773=PRODUCT('1/4-1/8 in port reducer (2)','1/4-1/8 in port reducer (2)',
'1/4-1/8 in port reducer (2)',(#5767));
#5847=COLOUR_RGB('Sky Blue',0.24,0.69,0.87);
#5848=FILL_AREA_STYLE_COLOUR('',#5847);
#5849=FILL_AREA_STYLE('',(#5848));
#5850=SURFACE_STYLE_FILL_AREA(#5849);
#5851=SURFACE_SIDE_STYLE('',(#5850));
#5852=SURFACE_STYLE_USAGE(.BOTH.,#5851);
#5853=PRESENTATION_STYLE_ASSIGNMENT((#5852));
ENDSEC;
END-ISO-10303-21;
